ISO-10303-21;
HEADER;
FILE_DESCRIPTION (('STEP AP214'),
    '1' );
FILE_NAME ('socket set screw cone point_iso_ISO 4027 - M4 x 16-N.step',
    '2026-10-04T07:23:31',
    ( '' ),
    ( '' ),
    'SwSTEP 2.0',
    'SolidWorks 2026',
    '' );
FILE_SCHEMA (( 'AUTOMOTIVE_DESIGN' ));
ENDSEC;

DATA;
#30=VECTOR ( 'NONE', #2527, 1000.000000000000000 ) ;
#37=PLANE ( 'NONE',  #10541 ) ;
#43=CARTESIAN_POINT ( 'NONE',  ( 0.2251666049839524120, 2.449293598294711838E-16, 2.000000000000004441 ) ) ;
#131=ORIENTED_EDGE ( 'NONE', *, *, #4600, .T. ) ;
#178=AXIS2_PLACEMENT_3D ( 'NONE', #3237, #7515, #1602 ) ;
#182=EDGE_CURVE ( 'NONE', #2588, #10522, #9482, .T. ) ;
#226=ORIENTED_EDGE ( 'NONE', *, *, #6126, .T. ) ;
#279=ADVANCED_FACE ( 'NONE', ( #7206 ), #1724, .T. ) ;
#295=CARTESIAN_POINT ( 'NONE',  ( 2.500000000000000444, -1.000000000000003109, -0.5773502691896260641 ) ) ;
#337=AXIS2_PLACEMENT_3D ( 'NONE', #6106, #5930, #7751 ) ;
#445=( NAMED_UNIT ( * ) SI_UNIT ( $, .STERADIAN. ) SOLID_ANGLE_UNIT ( ) );
#468=CARTESIAN_POINT ( 'NONE',  ( 2.500000000000000444, 1.000000000000002220, -0.5773502691896270633 ) ) ;
#482=CARTESIAN_POINT ( 'NONE',  ( 2.500000000000000444, -1.000000000000003331, 0.5773502691896272854 ) ) ;
#494=PRESENTATION_STYLE_ASSIGNMENT (( #8112 ) ) ;
#495=CARTESIAN_POINT ( 'NONE',  ( -12.69999999999998153, 0.000000000000000000, 0.000000000000000000 ) ) ;
#532=VECTOR ( 'NONE', #6272, 1000.000000000000227 ) ;
#585=EDGE_CURVE ( 'NONE', #6763, #4029, #1905, .T. ) ;
#591=EDGE_CURVE ( 'NONE', #811, #698, #1969, .T. ) ;
#597=ORIENTED_EDGE ( 'NONE', *, *, #2649, .F. ) ;
#647=ORIENTED_EDGE ( 'NONE', *, *, #6126, .F. ) ;
#698=VERTEX_POINT ( 'NONE', #1341 ) ;
#705=EDGE_LOOP ( 'NONE', ( #4344, #10523, #4176, #8992 ) ) ;
#727=EDGE_CURVE ( 'NONE', #698, #5070, #8800, .T. ) ;
#811=VERTEX_POINT ( 'NONE', #2974 ) ;
#820=FACE_BOUND ( 'NONE', #8065, .T. ) ;
#870=ORIENTED_EDGE ( 'NONE', *, *, #5978, .F. ) ;
#873=DIRECTION ( 'NONE',  ( -1.000000000000000000, 0.000000000000000000, 0.000000000000000000 ) ) ;
#908=SURFACE_STYLE_FILL_AREA ( #4116 ) ;
#945=CARTESIAN_POINT ( 'NONE',  ( 14.00000000000000533, 0.000000000000000000, 2.000000000000004441 ) ) ;
#957=LINE ( 'NONE', #9457, #7069 ) ;
#991=PLANE ( 'NONE',  #10921 ) ;
#1116=VECTOR ( 'NONE', #5042, 1000.000000000000227 ) ;
#1127=EDGE_CURVE ( 'NONE', #6508, #3052, #9847, .T. ) ;
#1154=CARTESIAN_POINT ( 'NONE',  ( -12.69999999999998153, 2.449293598294711838E-16, -2.000000000000004441 ) ) ;
#1207=DIRECTION ( 'NONE',  ( -1.000000000000000000, 0.000000000000000000, 0.000000000000000000 ) ) ;
#1210=ADVANCED_FACE ( 'NONE', ( #5028, #820 ), #991, .T. ) ;
#1274=DIRECTION ( 'NONE',  ( 0.000000000000000000, -0.4999999999999999445, -0.8660254037844387076 ) ) ;
#1318=ORIENTED_EDGE ( 'NONE', *, *, #1514, .F. ) ;
#1321=EDGE_CURVE ( 'NONE', #3052, #6508, #10023, .T. ) ;
#1341=CARTESIAN_POINT ( 'NONE',  ( 0.000000000000000000, 1.000000000000001998, 0.5773502691896277295 ) ) ;
#1428=ORIENTED_EDGE ( 'NONE', *, *, #8893, .T. ) ;
#1439=LINE ( 'NONE', #2167, #7262 ) ;
#1449=ORIENTED_EDGE ( 'NONE', *, *, #5130, .T. ) ;
#1459=DIRECTION ( 'NONE',  ( -1.000000000000000000, 0.000000000000000000, 0.000000000000000000 ) ) ;
#1488=ORIENTED_EDGE ( 'NONE', *, *, #7002, .F. ) ;
#1504=UNCERTAINTY_MEASURE_WITH_UNIT (LENGTH_MEASURE( 1.000000000000000082E-05 ), #9671, 'distance_accuracy_value', 'NONE');
#1506=DIRECTION ( 'NONE',  ( 0.000000000000000000, 0.000000000000000000, 1.000000000000000000 ) ) ;
#1514=EDGE_CURVE ( 'NONE', #4593, #7190, #7098, .T. ) ;
#1546=EDGE_LOOP ( 'NONE', ( #1782, #8978, #2188, #647 ) ) ;
#1587=APPLICATION_CONTEXT ( 'automotive_design' ) ;
#1602=DIRECTION ( 'NONE',  ( 0.000000000000000000, -0.8660254037844387076, 0.5000000000000001110 ) ) ;
#1609=EDGE_CURVE ( 'NONE', #5353, #2588, #2732, .T. ) ;
#1650=FACE_OUTER_BOUND ( 'NONE', #9279, .T. ) ;
#1679=SURFACE_STYLE_USAGE ( .BOTH. , #9957 ) ;
#1681=CARTESIAN_POINT ( 'NONE',  ( 14.00000000000000533, 2.449293598294706907E-16, -2.000000000000000000 ) ) ;
#1691=DIRECTION ( 'NONE',  ( 0.000000000000000000, 1.000000000000000000, 0.000000000000000000 ) ) ;
#1697=CARTESIAN_POINT ( 'NONE',  ( 0.000000000000000000, 0.000000000000000000, 0.000000000000000000 ) ) ;
#1718=DIRECTION ( 'NONE',  ( 0.000000000000000000, 0.4999999999999992228, -0.8660254037844391517 ) ) ;
#1724=CONICAL_SURFACE ( 'NONE', #6487, 1.610000000000003872, 1.047197551196600518 ) ;
#1730=( LENGTH_UNIT ( ) NAMED_UNIT ( * ) SI_UNIT ( .MILLI., .METRE. ) );
#1782=ORIENTED_EDGE ( 'NONE', *, *, #1321, .F. ) ;
#1820=CARTESIAN_POINT ( 'NONE',  ( 0.2251666049839524120, 0.000000000000000000, 0.000000000000000000 ) ) ;
#1835=DIRECTION ( 'NONE',  ( 0.000000000000000000, 0.000000000000000000, 1.000000000000000000 ) ) ;
#1836=ORIENTED_EDGE ( 'NONE', *, *, #9427, .T. ) ;
#1866=LINE ( 'NONE', #5248, #3210 ) ;
#1904=CARTESIAN_POINT ( 'NONE',  ( 0.000000000000000000, 0.000000000000000000, 0.000000000000000000 ) ) ;
#1905=LINE ( 'NONE', #10303, #10552 ) ;
#1917=DIRECTION ( 'NONE',  ( 0.000000000000000000, 0.000000000000000000, -1.000000000000000000 ) ) ;
#1930=CARTESIAN_POINT ( 'NONE',  ( 0.000000000000000000, 1.971681346627243419E-16, 1.610000000000003872 ) ) ;
#1956=ORIENTED_EDGE ( 'NONE', *, *, #7453, .F. ) ;
#1969=LINE ( 'NONE', #9351, #5442 ) ;
#2017=CONICAL_SURFACE ( 'NONE', #5011, 2.000000000000004441, 0.7853981633974496113 ) ;
#2025=LINE ( 'NONE', #3551, #3147 ) ;
#2079=AXIS2_PLACEMENT_3D ( 'NONE', #1820, #873, #4422 ) ;
#2089=AXIS2_PLACEMENT_3D ( 'NONE', #8010, #2142, #5523 ) ;
#2135=FACE_OUTER_BOUND ( 'NONE', #5942, .T. ) ;
#2142=DIRECTION ( 'NONE',  ( -1.000000000000000000, 0.000000000000000000, 0.000000000000000000 ) ) ;
#2167=CARTESIAN_POINT ( 'NONE',  ( 2.500000000000000444, -1.000000000000003331, 0.5773502691896272854 ) ) ;
#2188=ORIENTED_EDGE ( 'NONE', *, *, #10095, .T. ) ;
#2198=CARTESIAN_POINT ( 'NONE',  ( 0.000000000000000000, 1.000000000000002220, -0.5773502691896270633 ) ) ;
#2203=( NAMED_UNIT ( * ) SI_UNIT ( $, .STERADIAN. ) SOLID_ANGLE_UNIT ( ) );
#2256=ORIENTED_EDGE ( 'NONE', *, *, #727, .T. ) ;
#2261=ADVANCED_FACE ( 'NONE', ( #8449 ), #10119, .F. ) ;
#2278=UNCERTAINTY_MEASURE_WITH_UNIT (LENGTH_MEASURE( 1.000000000000000082E-05 ), #6262, 'distance_accuracy_value', 'NONE');
#2288=CARTESIAN_POINT ( 'NONE',  ( 2.500000000000000444, -4.336808689942017736E-16, 1.154700538379254571 ) ) ;
#2302=VECTOR ( 'NONE', #8664, 1000.000000000000227 ) ;
#2308=LINE ( 'NONE', #3173, #8174 ) ;
#2333=VECTOR ( 'NONE', #1917, 1000.000000000000000 ) ;
#2369=EDGE_LOOP ( 'NONE', ( #10597, #3470, #2844, #1318, #1488, #8708 ) ) ;
#2436=CARTESIAN_POINT ( 'NONE',  ( -12.69999999999998153, 0.000000000000000000, 0.000000000000000000 ) ) ;
#2474=ORIENTED_EDGE ( 'NONE', *, *, #591, .F. ) ;
#2487=LINE ( 'NONE', #6775, #5340 ) ;
#2507=AXIS2_PLACEMENT_3D ( 'NONE', #495, #10606, #3018 ) ;
#2527=DIRECTION ( 'NONE',  ( 0.000000000000000000, 0.8660254037844385966, 0.5000000000000001110 ) ) ;
#2537=ORIENTED_EDGE ( 'NONE', *, *, #182, .T. ) ;
#2588=VERTEX_POINT ( 'NONE', #1681 ) ;
#2589=ORIENTED_EDGE ( 'NONE', *, *, #1321, .T. ) ;
#2649=EDGE_CURVE ( 'NONE', #811, #8502, #2025, .T. ) ;
#2660=LINE ( 'NONE', #9418, #9403 ) ;
#2732=LINE ( 'NONE', #2783, #6719 ) ;
#2769=CIRCLE ( 'NONE', #2079, 2.000000000000004441 ) ;
#2783=CARTESIAN_POINT ( 'NONE',  ( 14.00000000000000533, 2.449293598294711838E-16, -2.000000000000004441 ) ) ;
#2829=ORIENTED_EDGE ( 'NONE', *, *, #3893, .F. ) ;
#2844=ORIENTED_EDGE ( 'NONE', *, *, #3505, .T. ) ;
#2957=ORIENTED_EDGE ( 'NONE', *, *, #6201, .F. ) ;
#2959=FILL_AREA_STYLE ('',( #5582 ) ) ;
#2974=CARTESIAN_POINT ( 'NONE',  ( 2.500000000000000444, 1.000000000000001998, 0.5773502691896277295 ) ) ;
#2987=AXIS2_PLACEMENT_3D ( 'NONE', #4656, #1274, #3760 ) ;
#3017=SURFACE_STYLE_FILL_AREA ( #2959 ) ;
#3018=DIRECTION ( 'NONE',  ( 0.000000000000000000, 0.000000000000000000, 1.000000000000000000 ) ) ;
#3045=CARTESIAN_POINT ( 'NONE',  ( 0.000000000000000000, -4.336808689942017736E-16, 1.154700538379254571 ) ) ;
#3046=CARTESIAN_POINT ( 'NONE',  ( 2.500000000000000444, -1.000000000000003331, 0.5773502691896272854 ) ) ;
#3052=VERTEX_POINT ( 'NONE', #6804 ) ;
#3073=DIRECTION ( 'NONE',  ( 0.000000000000000000, -0.8660254037844387076, 0.4999999999999999445 ) ) ;
#3120=LINE ( 'NONE', #4814, #10645 ) ;
#3147=VECTOR ( 'NONE', #8578, 1000.000000000000000 ) ;
#3173=CARTESIAN_POINT ( 'NONE',  ( 0.000000000000000000, 1.000000000000001998, 0.5773502691896277295 ) ) ;
#3180=ADVANCED_FACE ( 'NONE', ( #8011 ), #4502, .T. ) ;
#3210=VECTOR ( 'NONE', #8594, 1000.000000000000000 ) ;
#3214=CARTESIAN_POINT ( 'NONE',  ( 0.000000000000000000, -1.000000000000003331, 0.5773502691896272854 ) ) ;
#3237=CARTESIAN_POINT ( 'NONE',  ( 2.500000000000000444, -1.000000000000003109, -0.5773502691896260641 ) ) ;
#3286=CLOSED_SHELL ( 'NONE', ( #9644, #10839, #279, #1210, #7602, #7468, #7615, #3180, #10654, #7942, #3743, #2261, #4847, #9466 ) ) ;
#3297=LINE ( 'NONE', #10895, #6250 ) ;
#3395=AXIS2_PLACEMENT_3D ( 'NONE', #5897, #1691, #5073 ) ;
#3415=EDGE_LOOP ( 'NONE', ( #7848, #2537, #5153, #2829 ) ) ;
#3431=DIRECTION ( 'NONE',  ( 0.000000000000000000, 0.000000000000000000, 1.000000000000000000 ) ) ;
#3439=ORIENTED_EDGE ( 'NONE', *, *, #727, .F. ) ;
#3441=ORIENTED_EDGE ( 'NONE', *, *, #1609, .T. ) ;
#3470=ORIENTED_EDGE ( 'NONE', *, *, #2649, .T. ) ;
#3505=EDGE_CURVE ( 'NONE', #8502, #7190, #8039, .T. ) ;
#3541=ORIENTED_EDGE ( 'NONE', *, *, #10104, .T. ) ;
#3551=CARTESIAN_POINT ( 'NONE',  ( 2.500000000000000444, 1.000000000000001998, 0.5773502691896277295 ) ) ;
#3573=EDGE_CURVE ( 'NONE', #3052, #7535, #8086, .T. ) ;
#3608=DIRECTION ( 'NONE',  ( -1.000000000000000000, 0.000000000000000000, 0.000000000000000000 ) ) ;
#3678=COLOUR_RGB ( '', 0.66274510, 0.83137255, 0.94901961) ;
#3743=ADVANCED_FACE ( 'NONE', ( #6585 ), #8391, .T. ) ;
#3760=DIRECTION ( 'NONE',  ( 0.000000000000000000, 0.8660254037844387076, -0.4999999999999999445 ) ) ;
#3783=DIRECTION ( 'NONE',  ( 0.000000000000000000, -0.8660254037844387076, 0.4999999999999999445 ) ) ;
#3834=MECHANICAL_DESIGN_GEOMETRIC_PRESENTATION_REPRESENTATION('',(#8942),#6887);
#3841=CARTESIAN_POINT ( 'NONE',  ( 14.00000000000000533, 0.000000000000000000, 0.000000000000000000 ) ) ;
#3860=ORIENTED_EDGE ( 'NONE', *, *, #10607, .F. ) ;
#3866=( NAMED_UNIT ( * ) PLANE_ANGLE_UNIT ( ) SI_UNIT ( $, .RADIAN. ) );
#3893=EDGE_CURVE ( 'NONE', #5479, #7535, #957, .T. ) ;
#3912=DIRECTION ( 'NONE',  ( 0.000000000000000000, 1.000000000000000000, 0.000000000000000000 ) ) ;
#3923=AXIS2_PLACEMENT_3D ( 'NONE', #9166, #6806, #1835 ) ;
#4020=PLANE ( 'NONE',  #6753 ) ;
#4029=VERTEX_POINT ( 'NONE', #8786 ) ;
#4057=FACE_OUTER_BOUND ( 'NONE', #3415, .T. ) ;
#4078=CARTESIAN_POINT ( 'NONE',  ( 2.500000000000000444, -1.000000000000003109, -0.5773502691896260641 ) ) ;
#4110=ORIENTED_EDGE ( 'NONE', *, *, #7453, .T. ) ;
#4116=FILL_AREA_STYLE ('',( #9180 ) ) ;
#4141=CARTESIAN_POINT ( 'NONE',  ( 0.2251666049839524120, 0.000000000000000000, -2.000000000000004441 ) ) ;
#4169=DIRECTION ( 'NONE',  ( -0.7071067811865457964, 0.000000000000000000, 0.7071067811865492381 ) ) ;
#4173=ORIENTED_EDGE ( 'NONE', *, *, #7132, .T. ) ;
#4174=ORIENTED_EDGE ( 'NONE', *, *, #7002, .T. ) ;
#4176=ORIENTED_EDGE ( 'NONE', *, *, #3505, .F. ) ;
#4197=( GEOMETRIC_REPRESENTATION_CONTEXT ( 3 ) GLOBAL_UNCERTAINTY_ASSIGNED_CONTEXT ( ( #4843 ) ) GLOBAL_UNIT_ASSIGNED_CONTEXT ( ( #1730, #8459, #10907 ) ) REPRESENTATION_CONTEXT ( 'NONE', 'WORKASPACE' ) );
#4201=CARTESIAN_POINT ( 'NONE',  ( 0.000000000000000000, 0.000000000000000000, -1.610000000000003872 ) ) ;
#4209=EDGE_LOOP ( 'NONE', ( #4110, #870, #597, #6691 ) ) ;
#4216=CYLINDRICAL_SURFACE ( 'NONE', #9308, 2.000000000000004441 ) ;
#4246=CARTESIAN_POINT ( 'NONE',  ( 0.000000000000000000, 0.000000000000000000, -1.610000000000000320 ) ) ;
#4291=AXIS2_PLACEMENT_3D ( 'NONE', #7056, #10412, #5401 ) ;
#4344=ORIENTED_EDGE ( 'NONE', *, *, #10386, .T. ) ;
#4364=DIRECTION ( 'NONE',  ( 0.000000000000000000, 0.000000000000000000, 1.000000000000000000 ) ) ;
#4414=ADVANCED_BREP_SHAPE_REPRESENTATION ( '', ( #10772, #7040 ), #8779 ) ;
#4422=DIRECTION ( 'NONE',  ( 0.000000000000000000, 0.000000000000000000, 1.000000000000000000 ) ) ;
#4479=CONICAL_SURFACE ( 'NONE', #4641, 2.000000000000004441, 0.7853981633974496113 ) ;
#4502=PLANE ( 'NONE',  #2987 ) ;
#4543=EDGE_LOOP ( 'NONE', ( #6622, #7204, #6247 ) ) ;
#4557=( NAMED_UNIT ( * ) PLANE_ANGLE_UNIT ( ) SI_UNIT ( $, .RADIAN. ) );
#4576=VECTOR ( 'NONE', #8603, 1000.000000000000000 ) ;
#4593=VERTEX_POINT ( 'NONE', #7946 ) ;
#4596=LINE ( 'NONE', #9705, #6256 ) ;
#4600=EDGE_CURVE ( 'NONE', #9751, #5070, #4596, .T. ) ;
#4641=AXIS2_PLACEMENT_3D ( 'NONE', #8596, #1207, #8767 ) ;
#4656=CARTESIAN_POINT ( 'NONE',  ( 2.500000000000000444, 1.000000000000001998, 0.5773502691896277295 ) ) ;
#4695=EDGE_LOOP ( 'NONE', ( #3439, #2474, #8037, #131 ) ) ;
#4698=DIRECTION ( 'NONE',  ( -1.000000000000000000, 0.000000000000000000, 0.000000000000000000 ) ) ;
#4710=FACE_OUTER_BOUND ( 'NONE', #6173, .T. ) ;
#4741=MECHANICAL_DESIGN_GEOMETRIC_PRESENTATION_REPRESENTATION('',(#9679),#4197);
#4757=SHAPE_REPRESENTATION_RELATIONSHIP ( 'NONE' , 'NONE' ,  #9997, #4414 ) ;
#4783=DIRECTION ( 'NONE',  ( 0.000000000000000000, 0.000000000000000000, -1.000000000000000000 ) ) ;
#4814=CARTESIAN_POINT ( 'NONE',  ( 2.500000000000000444, 1.000000000000001998, 0.5773502691896277295 ) ) ;
#4833=DIRECTION ( 'NONE',  ( -1.000000000000000000, 0.000000000000000000, 0.000000000000000000 ) ) ;
#4843=UNCERTAINTY_MEASURE_WITH_UNIT (LENGTH_MEASURE( 1.000000000000000082E-05 ), #1730, 'distance_accuracy_value', 'NONE');
#4847=ADVANCED_FACE ( 'NONE', ( #6785 ), #10870, .F. ) ;
#4899=VECTOR ( 'NONE', #6065, 1000.000000000000000 ) ;
#4949=EDGE_LOOP ( 'NONE', ( #10742, #3441, #2957 ) ) ;
#4955=ORIENTED_EDGE ( 'NONE', *, *, #8893, .F. ) ;
#4965=DIRECTION ( 'NONE',  ( 0.000000000000000000, 0.000000000000000000, -1.000000000000000000 ) ) ;
#5011=AXIS2_PLACEMENT_3D ( 'NONE', #10100, #9153, #4364 ) ;
#5028=FACE_OUTER_BOUND ( 'NONE', #6330, .T. ) ;
#5033=PRODUCT_CONTEXT ( 'NONE', #1587, 'mechanical' ) ;
#5042=DIRECTION ( 'NONE',  ( 0.4999999999999967248, 0.000000000000000000, -0.8660254037844404840 ) ) ;
#5070=VERTEX_POINT ( 'NONE', #3045 ) ;
#5073=DIRECTION ( 'NONE',  ( 0.000000000000000000, 0.000000000000000000, 1.000000000000000000 ) ) ;
#5129=PLANE ( 'NONE',  #9198 ) ;
#5130=EDGE_CURVE ( 'NONE', #2588, #5479, #8355, .T. ) ;
#5153=ORIENTED_EDGE ( 'NONE', *, *, #10095, .F. ) ;
#5248=CARTESIAN_POINT ( 'NONE',  ( 2.500000000000000444, 1.000000000000002220, -0.5773502691896270633 ) ) ;
#5340=VECTOR ( 'NONE', #4169, 1000.000000000000000 ) ;
#5353=VERTEX_POINT ( 'NONE', #10711 ) ;
#5401=DIRECTION ( 'NONE',  ( 0.000000000000000000, 0.000000000000000000, 1.000000000000000000 ) ) ;
#5442=VECTOR ( 'NONE', #3608, 1000.000000000000000 ) ;
#5479=VERTEX_POINT ( 'NONE', #945 ) ;
#5523=DIRECTION ( 'NONE',  ( 0.000000000000000000, 0.000000000000000000, 1.000000000000000000 ) ) ;
#5582=FILL_AREA_STYLE_COLOUR ( '', #10186 ) ;
#5607=CARTESIAN_POINT ( 'NONE',  ( 0.000000000000000000, 0.000000000000000000, 0.000000000000000000 ) ) ;
#5760=DIRECTION ( 'NONE',  ( -1.000000000000000000, 0.000000000000000000, 0.000000000000000000 ) ) ;
#5792=DIRECTION ( 'NONE',  ( 0.000000000000000000, 0.000000000000000000, -1.000000000000000000 ) ) ;
#5893=VERTEX_POINT ( 'NONE', #9248 ) ;
#5897=CARTESIAN_POINT ( 'NONE',  ( 2.500000000000000444, 1.000000000000001998, 0.5773502691896277295 ) ) ;
#5919=ORIENTED_EDGE ( 'NONE', *, *, #3893, .T. ) ;
#5930=DIRECTION ( 'NONE',  ( -1.000000000000000000, 0.000000000000000000, 0.000000000000000000 ) ) ;
#5942=EDGE_LOOP ( 'NONE', ( #6372, #4955, #4174, #1836 ) ) ;
#5963=VECTOR ( 'NONE', #9767, 999.9999999999998863 ) ;
#5974=LINE ( 'NONE', #4201, #1116 ) ;
#5978=EDGE_CURVE ( 'NONE', #8502, #5893, #1866, .T. ) ;
#6016=EDGE_LOOP ( 'NONE', ( #6355, #6789, #9420, #3541 ) ) ;
#6065=DIRECTION ( 'NONE',  ( -1.000000000000000000, 0.000000000000000000, 0.000000000000000000 ) ) ;
#6106=CARTESIAN_POINT ( 'NONE',  ( 0.000000000000000000, 0.000000000000000000, 0.000000000000000000 ) ) ;
#6126=EDGE_CURVE ( 'NONE', #6508, #10522, #5974, .T. ) ;
#6173=EDGE_LOOP ( 'NONE', ( #8247, #1449, #5919, #3860 ) ) ;
#6201=EDGE_CURVE ( 'NONE', #5479, #2588, #9385, .T. ) ;
#6216=EDGE_CURVE ( 'NONE', #8398, #9751, #10111, .T. ) ;
#6247=ORIENTED_EDGE ( 'NONE', *, *, #5130, .F. ) ;
#6250=VECTOR ( 'NONE', #9328, 1000.000000000000227 ) ;
#6256=VECTOR ( 'NONE', #4698, 1000.000000000000000 ) ;
#6262=( LENGTH_UNIT ( ) NAMED_UNIT ( * ) SI_UNIT ( .MILLI., .METRE. ) );
#6272=DIRECTION ( 'NONE',  ( 0.000000000000000000, 0.8660254037844385966, -0.4999999999999998890 ) ) ;
#6284=PRODUCT ( 'socket set screw cone point_iso_ISO 4027 - M4 x 16-N', 'socket set screw cone point_iso_ISO 4027 - M4 x 16-N', '', ( #5033 ) ) ;
#6330=EDGE_LOOP ( 'NONE', ( #8706, #2589 ) ) ;
#6355=ORIENTED_EDGE ( 'NONE', *, *, #7132, .F. ) ;
#6364=SURFACE_SIDE_STYLE ('',( #3017 ) ) ;
#6372=ORIENTED_EDGE ( 'NONE', *, *, #585, .F. ) ;
#6487=AXIS2_PLACEMENT_3D ( 'NONE', #5607, #8967, #4783 ) ;
#6499=VECTOR ( 'NONE', #3783, 999.9999999999998863 ) ;
#6508=VERTEX_POINT ( 'NONE', #4246 ) ;
#6585=FACE_OUTER_BOUND ( 'NONE', #6016, .T. ) ;
#6622=ORIENTED_EDGE ( 'NONE', *, *, #1609, .F. ) ;
#6679=ORIENTED_EDGE ( 'NONE', *, *, #3573, .F. ) ;
#6691=ORIENTED_EDGE ( 'NONE', *, *, #591, .T. ) ;
#6696=CARTESIAN_POINT ( 'NONE',  ( 2.500000000000000444, -1.000000000000003331, 0.5773502691896272854 ) ) ;
#6719=VECTOR ( 'NONE', #10258, 1000.000000000000000 ) ;
#6739=FACE_OUTER_BOUND ( 'NONE', #4543, .T. ) ;
#6753=AXIS2_PLACEMENT_3D ( 'NONE', #482, #3912, #10746 ) ;
#6754=CARTESIAN_POINT ( 'NONE',  ( 2.500000000000000444, -6.505213034913026604E-16, -1.154700538379252794 ) ) ;
#6763=VERTEX_POINT ( 'NONE', #3214 ) ;
#6775=CARTESIAN_POINT ( 'NONE',  ( 14.00000000000000533, 0.000000000000000000, 2.000000000000004441 ) ) ;
#6785=FACE_OUTER_BOUND ( 'NONE', #4209, .T. ) ;
#6789=ORIENTED_EDGE ( 'NONE', *, *, #9427, .F. ) ;
#6804=CARTESIAN_POINT ( 'NONE',  ( 0.000000000000000000, 2.210487472460972698E-16, 1.610000000000000320 ) ) ;
#6806=DIRECTION ( 'NONE',  ( -1.000000000000000000, 0.000000000000000000, 0.000000000000000000 ) ) ;
#6816=ORIENTED_EDGE ( 'NONE', *, *, #6216, .F. ) ;
#6825=DIRECTION ( 'NONE',  ( 0.000000000000000000, 0.000000000000000000, -1.000000000000000000 ) ) ;
#6840=FACE_OUTER_BOUND ( 'NONE', #2369, .T. ) ;
#6887=( GEOMETRIC_REPRESENTATION_CONTEXT ( 3 ) GLOBAL_UNCERTAINTY_ASSIGNED_CONTEXT ( ( #1504 ) ) GLOBAL_UNIT_ASSIGNED_CONTEXT ( ( #9671, #4557, #2203 ) ) REPRESENTATION_CONTEXT ( 'NONE', 'WORKASPACE' ) );
#6910=DIRECTION ( 'NONE',  ( -1.000000000000000000, 0.000000000000000000, 0.000000000000000000 ) ) ;
#6993=DIRECTION ( 'NONE',  ( -1.000000000000000000, 0.000000000000000000, 0.000000000000000000 ) ) ;
#7002=EDGE_CURVE ( 'NONE', #8398, #4593, #9484, .T. ) ;
#7040=AXIS2_PLACEMENT_3D ( 'NONE', #1904, #3431, #7048 ) ;
#7048=DIRECTION ( 'NONE',  ( 1.000000000000000000, 0.000000000000000000, 0.000000000000000000 ) ) ;
#7056=CARTESIAN_POINT ( 'NONE',  ( 0.2251666049839524120, 0.000000000000000000, 0.000000000000000000 ) ) ;
#7069=VECTOR ( 'NONE', #10341, 1000.000000000000000 ) ;
#7098=LINE ( 'NONE', #295, #532 ) ;
#7132=EDGE_CURVE ( 'NONE', #4029, #7313, #3297, .T. ) ;
#7134=ORIENTED_EDGE ( 'NONE', *, *, #1127, .F. ) ;
#7190=VERTEX_POINT ( 'NONE', #6754 ) ;
#7204=ORIENTED_EDGE ( 'NONE', *, *, #8543, .T. ) ;
#7206=FACE_OUTER_BOUND ( 'NONE', #1546, .T. ) ;
#7230=DIRECTION ( 'NONE',  ( 0.000000000000000000, 0.000000000000000000, -1.000000000000000000 ) ) ;
#7255=DIRECTION ( 'NONE',  ( 0.000000000000000000, -0.8660254037844387076, -0.5000000000000001110 ) ) ;
#7262=VECTOR ( 'NONE', #4833, 1000.000000000000000 ) ;
#7299=CARTESIAN_POINT ( 'NONE',  ( 0.000000000000000000, 1.000000000000001998, 0.5773502691896277295 ) ) ;
#7313=VERTEX_POINT ( 'NONE', #10551 ) ;
#7332=SHAPE_DEFINITION_REPRESENTATION ( #10416, #9997 ) ;
#7355=EDGE_CURVE ( 'NONE', #811, #9751, #3120, .T. ) ;
#7357=DIRECTION ( 'NONE',  ( 0.000000000000000000, -0.5000000000000001110, 0.8660254037844387076 ) ) ;
#7440=APPLICATION_CONTEXT ( 'automotive_design' ) ;
#7453=EDGE_CURVE ( 'NONE', #698, #5893, #2308, .T. ) ;
#7468=ADVANCED_FACE ( 'NONE', ( #4710 ), #8057, .T. ) ;
#7512=PRODUCT_DEFINITION ( 'UNKNOWN', '', #10401, #10793 ) ;
#7515=DIRECTION ( 'NONE',  ( 0.000000000000000000, 0.5000000000000001110, 0.8660254037844387076 ) ) ;
#7528=PRESENTATION_STYLE_ASSIGNMENT (( #1679 ) ) ;
#7535=VERTEX_POINT ( 'NONE', #43 ) ;
#7602=ADVANCED_FACE ( 'NONE', ( #1650 ), #7645, .T. ) ;
#7604=FACE_OUTER_BOUND ( 'NONE', #9552, .T. ) ;
#7615=ADVANCED_FACE ( 'NONE', ( #6739 ), #2017, .T. ) ;
#7645=CONICAL_SURFACE ( 'NONE', #10296, 1.610000000000003872, 1.047197551196600518 ) ;
#7673=CARTESIAN_POINT ( 'NONE',  ( 0.000000000000000000, 0.000000000000000000, 0.000000000000000000 ) ) ;
#7712=CARTESIAN_POINT ( 'NONE',  ( 2.500000000000000444, -1.000000000000003331, 0.5773502691896272854 ) ) ;
#7748=ORIENTED_EDGE ( 'NONE', *, *, #10583, .F. ) ;
#7751=DIRECTION ( 'NONE',  ( 0.000000000000000000, 0.000000000000000000, 1.000000000000000000 ) ) ;
#7840=FACE_OUTER_BOUND ( 'NONE', #4949, .T. ) ;
#7848=ORIENTED_EDGE ( 'NONE', *, *, #6201, .T. ) ;
#7942=ADVANCED_FACE ( 'NONE', ( #2135 ), #4020, .T. ) ;
#7946=CARTESIAN_POINT ( 'NONE',  ( 2.500000000000000444, -1.000000000000003109, -0.5773502691896260641 ) ) ;
#7998=CIRCLE ( 'NONE', #4291, 2.000000000000004441 ) ;
#8010=CARTESIAN_POINT ( 'NONE',  ( 0.000000000000000000, 0.000000000000000000, 0.000000000000000000 ) ) ;
#8011=FACE_OUTER_BOUND ( 'NONE', #4695, .T. ) ;
#8037=ORIENTED_EDGE ( 'NONE', *, *, #7355, .T. ) ;
#8039=LINE ( 'NONE', #468, #9002 ) ;
#8057=CYLINDRICAL_SURFACE ( 'NONE', #2507, 2.000000000000004441 ) ;
#8065=EDGE_LOOP ( 'NONE', ( #1956, #2256, #7748, #8084, #4173, #9969 ) ) ;
#8084=ORIENTED_EDGE ( 'NONE', *, *, #585, .T. ) ;
#8086=LINE ( 'NONE', #1930, #2302 ) ;
#8089=DIRECTION ( 'NONE',  ( 0.000000000000000000, 0.000000000000000000, 1.000000000000000000 ) ) ;
#8112=SURFACE_STYLE_USAGE ( .BOTH. , #6364 ) ;
#8174=VECTOR ( 'NONE', #7230, 1000.000000000000000 ) ;
#8247=ORIENTED_EDGE ( 'NONE', *, *, #182, .F. ) ;
#8256=LINE ( 'NONE', #4078, #10088 ) ;
#8274=AXIS2_PLACEMENT_3D ( 'NONE', #8284, #1718, #10786 ) ;
#8284=CARTESIAN_POINT ( 'NONE',  ( 2.500000000000000444, 1.000000000000002220, -0.5773502691896270633 ) ) ;
#8355=CIRCLE ( 'NONE', #9422, 2.000000000000004441 ) ;
#8391=PLANE ( 'NONE',  #178 ) ;
#8398=VERTEX_POINT ( 'NONE', #3046 ) ;
#8424=CARTESIAN_POINT ( 'NONE',  ( 2.500000000000000444, -1.000000000000003109, 1.732050807568882078 ) ) ;
#8434=DIRECTION ( 'NONE',  ( 1.000000000000000000, 0.000000000000000000, 0.000000000000000000 ) ) ;
#8449=FACE_OUTER_BOUND ( 'NONE', #705, .T. ) ;
#8459=( NAMED_UNIT ( * ) PLANE_ANGLE_UNIT ( ) SI_UNIT ( $, .RADIAN. ) );
#8487=CARTESIAN_POINT ( 'NONE',  ( 0.000000000000000000, -1.000000000000003331, 0.5773502691896272854 ) ) ;
#8502=VERTEX_POINT ( 'NONE', #9289 ) ;
#8543=EDGE_CURVE ( 'NONE', #5353, #5479, #2487, .T. ) ;
#8578=DIRECTION ( 'NONE',  ( 0.000000000000000000, 0.000000000000000000, -1.000000000000000000 ) ) ;
#8594=DIRECTION ( 'NONE',  ( -1.000000000000000000, 0.000000000000000000, 0.000000000000000000 ) ) ;
#8596=CARTESIAN_POINT ( 'NONE',  ( 14.00000000000000533, 0.000000000000000000, 0.000000000000000000 ) ) ;
#8603=DIRECTION ( 'NONE',  ( 0.000000000000000000, 0.8660254037844385966, 0.5000000000000001110 ) ) ;
#8664=DIRECTION ( 'NONE',  ( 0.4999999999999967248, 1.060575238724909133E-16, 0.8660254037844404840 ) ) ;
#8706=ORIENTED_EDGE ( 'NONE', *, *, #1127, .T. ) ;
#8708=ORIENTED_EDGE ( 'NONE', *, *, #6216, .T. ) ;
#8767=DIRECTION ( 'NONE',  ( 0.000000000000000000, 0.000000000000000000, 1.000000000000000000 ) ) ;
#8779=( GEOMETRIC_REPRESENTATION_CONTEXT ( 3 ) GLOBAL_UNCERTAINTY_ASSIGNED_CONTEXT ( ( #2278 ) ) GLOBAL_UNIT_ASSIGNED_CONTEXT ( ( #6262, #3866, #445 ) ) REPRESENTATION_CONTEXT ( 'NONE', 'WORKASPACE' ) );
#8783=LINE ( 'NONE', #2198, #5963 ) ;
#8786=CARTESIAN_POINT ( 'NONE',  ( 0.000000000000000000, -1.000000000000003109, -0.5773502691896260641 ) ) ;
#8800=LINE ( 'NONE', #7299, #6499 ) ;
#8893=EDGE_CURVE ( 'NONE', #8398, #6763, #1439, .T. ) ;
#8914=DIRECTION ( 'NONE',  ( 0.000000000000000000, -0.8660254037844391517, -0.4999999999999992784 ) ) ;
#8942=STYLED_ITEM ( 'NONE', ( #494 ), #4414 ) ;
#8967=DIRECTION ( 'NONE',  ( 1.000000000000000000, 0.000000000000000000, 0.000000000000000000 ) ) ;
#8969=CARTESIAN_POINT ( 'NONE',  ( 2.500000000000000444, -1.000000000000003331, 0.5773502691896272854 ) ) ;
#8978=ORIENTED_EDGE ( 'NONE', *, *, #3573, .T. ) ;
#8992=ORIENTED_EDGE ( 'NONE', *, *, #5978, .T. ) ;
#9002=VECTOR ( 'NONE', #8914, 999.9999999999998863 ) ;
#9153=DIRECTION ( 'NONE',  ( -1.000000000000000000, 0.000000000000000000, 0.000000000000000000 ) ) ;
#9166=CARTESIAN_POINT ( 'NONE',  ( 14.00000000000000533, 0.000000000000000000, 0.000000000000000000 ) ) ;
#9180=FILL_AREA_STYLE_COLOUR ( '', #3678 ) ;
#9198=AXIS2_PLACEMENT_3D ( 'NONE', #8424, #10029, #4965 ) ;
#9248=CARTESIAN_POINT ( 'NONE',  ( 0.000000000000000000, 1.000000000000002220, -0.5773502691896270633 ) ) ;
#9279=EDGE_LOOP ( 'NONE', ( #6679, #7134, #226, #9654 ) ) ;
#9289=CARTESIAN_POINT ( 'NONE',  ( 2.500000000000000444, 1.000000000000002220, -0.5773502691896270633 ) ) ;
#9308=AXIS2_PLACEMENT_3D ( 'NONE', #2436, #5760, #1506 ) ;
#9328=DIRECTION ( 'NONE',  ( 0.000000000000000000, 0.8660254037844385966, -0.4999999999999998890 ) ) ;
#9351=CARTESIAN_POINT ( 'NONE',  ( 2.500000000000000444, 1.000000000000001998, 0.5773502691896277295 ) ) ;
#9377=LINE ( 'NONE', #8487, #4576 ) ;
#9385=CIRCLE ( 'NONE', #3923, 2.000000000000004441 ) ;
#9403=VECTOR ( 'NONE', #6993, 1000.000000000000000 ) ;
#9418=CARTESIAN_POINT ( 'NONE',  ( 2.500000000000000444, -6.505213034913026604E-16, -1.154700538379252794 ) ) ;
#9420=ORIENTED_EDGE ( 'NONE', *, *, #1514, .T. ) ;
#9422=AXIS2_PLACEMENT_3D ( 'NONE', #3841, #1459, #8089 ) ;
#9427=EDGE_CURVE ( 'NONE', #4593, #4029, #8256, .T. ) ;
#9457=CARTESIAN_POINT ( 'NONE',  ( -12.69999999999998153, 0.000000000000000000, 2.000000000000004441 ) ) ;
#9466=ADVANCED_FACE ( 'NONE', ( #6840 ), #5129, .F. ) ;
#9482=LINE ( 'NONE', #1154, #4899 ) ;
#9484=LINE ( 'NONE', #7712, #2333 ) ;
#9552=EDGE_LOOP ( 'NONE', ( #10798, #9825, #6816, #1428 ) ) ;
#9644=ADVANCED_FACE ( 'NONE', ( #7840 ), #4479, .T. ) ;
#9654=ORIENTED_EDGE ( 'NONE', *, *, #10607, .T. ) ;
#9671=( LENGTH_UNIT ( ) NAMED_UNIT ( * ) SI_UNIT ( .MILLI., .METRE. ) );
#9679=STYLED_ITEM ( 'NONE', ( #7528 ), #10772 ) ;
#9705=CARTESIAN_POINT ( 'NONE',  ( 2.500000000000000444, -4.336808689942017736E-16, 1.154700538379254571 ) ) ;
#9751=VERTEX_POINT ( 'NONE', #2288 ) ;
#9767=DIRECTION ( 'NONE',  ( 0.000000000000000000, -0.8660254037844391517, -0.4999999999999992784 ) ) ;
#9825=ORIENTED_EDGE ( 'NONE', *, *, #4600, .F. ) ;
#9847=CIRCLE ( 'NONE', #2089, 1.610000000000003872 ) ;
#9957=SURFACE_SIDE_STYLE ('',( #908 ) ) ;
#9969=ORIENTED_EDGE ( 'NONE', *, *, #10386, .F. ) ;
#9997=SHAPE_REPRESENTATION ( 'socket set screw cone point_iso_ISO 4027 - M4 x 16-N', ( #7040 ), #8779 ) ;
#10023=CIRCLE ( 'NONE', #337, 1.610000000000003872 ) ;
#10029=DIRECTION ( 'NONE',  ( 1.000000000000000000, 0.000000000000000000, 0.000000000000000000 ) ) ;
#10034=DIRECTION ( 'NONE',  ( 0.000000000000000000, 0.000000000000000000, 1.000000000000000000 ) ) ;
#10088=VECTOR ( 'NONE', #10815, 1000.000000000000000 ) ;
#10095=EDGE_CURVE ( 'NONE', #7535, #10522, #7998, .T. ) ;
#10100=CARTESIAN_POINT ( 'NONE',  ( 14.00000000000000533, 0.000000000000000000, 0.000000000000000000 ) ) ;
#10104=EDGE_CURVE ( 'NONE', #7190, #7313, #2660, .T. ) ;
#10111=LINE ( 'NONE', #6696, #30 ) ;
#10119=PLANE ( 'NONE',  #8274 ) ;
#10186=COLOUR_RGB ( '', 0.66274510, 0.83137255, 0.94901961) ;
#10258=DIRECTION ( 'NONE',  ( -0.7071067811865457964, 8.659560562354953812E-17, -0.7071067811865492381 ) ) ;
#10296=AXIS2_PLACEMENT_3D ( 'NONE', #7673, #8434, #5792 ) ;
#10303=CARTESIAN_POINT ( 'NONE',  ( 0.000000000000000000, -1.000000000000003331, 0.5773502691896272854 ) ) ;
#10341=DIRECTION ( 'NONE',  ( -1.000000000000000000, 0.000000000000000000, 0.000000000000000000 ) ) ;
#10386=EDGE_CURVE ( 'NONE', #5893, #7313, #8783, .T. ) ;
#10401=PRODUCT_DEFINITION_FORMATION_WITH_SPECIFIED_SOURCE ( 'ANY', '', #6284, .NOT_KNOWN. ) ;
#10412=DIRECTION ( 'NONE',  ( -1.000000000000000000, 0.000000000000000000, 0.000000000000000000 ) ) ;
#10416=PRODUCT_DEFINITION_SHAPE ( 'NONE', 'NONE',  #7512 ) ;
#10522=VERTEX_POINT ( 'NONE', #4141 ) ;
#10523=ORIENTED_EDGE ( 'NONE', *, *, #10104, .F. ) ;
#10541=AXIS2_PLACEMENT_3D ( 'NONE', #8969, #7357, #7255 ) ;
#10551=CARTESIAN_POINT ( 'NONE',  ( 0.000000000000000000, -6.505213034913026604E-16, -1.154700538379252794 ) ) ;
#10552=VECTOR ( 'NONE', #6825, 1000.000000000000000 ) ;
#10583=EDGE_CURVE ( 'NONE', #6763, #5070, #9377, .T. ) ;
#10597=ORIENTED_EDGE ( 'NONE', *, *, #7355, .F. ) ;
#10606=DIRECTION ( 'NONE',  ( -1.000000000000000000, 0.000000000000000000, 0.000000000000000000 ) ) ;
#10607=EDGE_CURVE ( 'NONE', #10522, #7535, #2769, .T. ) ;
#10645=VECTOR ( 'NONE', #3073, 999.9999999999998863 ) ;
#10654=ADVANCED_FACE ( 'NONE', ( #7604 ), #37, .F. ) ;
#10711=CARTESIAN_POINT ( 'NONE',  ( 16.00000000000000000, 0.000000000000000000, 0.000000000000000000 ) ) ;
#10742=ORIENTED_EDGE ( 'NONE', *, *, #8543, .F. ) ;
#10746=DIRECTION ( 'NONE',  ( 0.000000000000000000, 0.000000000000000000, 1.000000000000000000 ) ) ;
#10772=MANIFOLD_SOLID_BREP ( 'Hex', #3286 ) ;
#10786=DIRECTION ( 'NONE',  ( 0.000000000000000000, 0.8660254037844391517, 0.4999999999999992228 ) ) ;
#10793=PRODUCT_DEFINITION_CONTEXT ( 'detailed design', #7440, 'design' ) ;
#10798=ORIENTED_EDGE ( 'NONE', *, *, #10583, .T. ) ;
#10815=DIRECTION ( 'NONE',  ( -1.000000000000000000, 0.000000000000000000, 0.000000000000000000 ) ) ;
#10839=ADVANCED_FACE ( 'NONE', ( #4057 ), #4216, .T. ) ;
#10870=PLANE ( 'NONE',  #3395 ) ;
#10895=CARTESIAN_POINT ( 'NONE',  ( 0.000000000000000000, -1.000000000000003109, -0.5773502691896260641 ) ) ;
#10907=( NAMED_UNIT ( * ) SI_UNIT ( $, .STERADIAN. ) SOLID_ANGLE_UNIT ( ) );
#10921=AXIS2_PLACEMENT_3D ( 'NONE', #1697, #6910, #10034 ) ;
ENDSEC;
END-ISO-10303-21;
